ISO-10303-21;
HEADER;
/* Generated by software containing ST-Developer
 * from STEP Tools, Inc. (www.steptools.com) 
 */

FILE_DESCRIPTION(
/* description */ (''),
/* implementation_level */ '2;1');

FILE_NAME(
/* name */ '10_Axial_Preload_Shim_25x32x0.5.step',
/* time_stamp */ '2026-10-26T04:15:57-07:00',
/* author */ (''),
/* organization */ (''),
/* preprocessor_version */ 'ST-DEVELOPER v20.2',
/* originating_system */ 'Autodesk Translation Framework v15.15.0.0',
/* authorisation */ '');

FILE_SCHEMA (('AUTOMOTIVE_DESIGN { 1 0 10303 214 3 1 1 }'));
ENDSEC;

DATA;
#10=MECHANICAL_DESIGN_GEOMETRIC_PRESENTATION_REPRESENTATION('',(#461),#55737);
#421=SHAPE_REPRESENTATION_RELATIONSHIP('SRR','None',#55830,#441);
#441=ADVANCED_BREP_SHAPE_REPRESENTATION('',(#481),#55726);
#461=STYLED_ITEM('',(#56005),#481);
#481=MANIFOLD_SOLID_BREP('Body1',#27230);
#702=FACE_BOUND('',#9520,.T.);
#703=FACE_BOUND('',#9523,.T.);
#1395=PLANE('',#29191);
#1396=PLANE('',#29195);
#3338=LINE('',#45264,#5709);
#3339=LINE('',#45272,#5710);
#5709=VECTOR('',#35012,12.55);
#5710=VECTOR('',#35023,16.);
#6692=CYLINDRICAL_SURFACE('',#29188,12.55);
#6693=CYLINDRICAL_SURFACE('',#29193,16.);
#7851=FACE_OUTER_BOUND('',#9518,.T.);
#7852=FACE_OUTER_BOUND('',#9519,.T.);
#7853=FACE_OUTER_BOUND('',#9521,.T.);
#7854=FACE_OUTER_BOUND('',#9522,.T.);
#9518=EDGE_LOOP('',(#22990,#22991,#22992,#22993));
#9519=EDGE_LOOP('',(#22994));
#9520=EDGE_LOOP('',(#22995));
#9521=EDGE_LOOP('',(#22996,#22997,#22998,#22999));
#9522=EDGE_LOOP('',(#23000));
#9523=EDGE_LOOP('',(#23001));
#10776=CIRCLE('',#29189,12.55);
#10777=CIRCLE('',#29190,12.55);
#10778=CIRCLE('',#29192,16.);
#10779=CIRCLE('',#29194,16.);
#13087=VERTEX_POINT('',#45261);
#13088=VERTEX_POINT('',#45263);
#13089=VERTEX_POINT('',#45267);
#13090=VERTEX_POINT('',#45270);
#16499=EDGE_CURVE('',#13087,#13087,#10776,.T.);
#16500=EDGE_CURVE('',#13087,#13088,#3338,.T.);
#16501=EDGE_CURVE('',#13088,#13088,#10777,.T.);
#16502=EDGE_CURVE('',#13089,#13089,#10778,.T.);
#16503=EDGE_CURVE('',#13090,#13090,#10779,.T.);
#16504=EDGE_CURVE('',#13090,#13089,#3339,.T.);
#22990=ORIENTED_EDGE('',*,*,#16499,.T.);
#22991=ORIENTED_EDGE('',*,*,#16500,.T.);
#22992=ORIENTED_EDGE('',*,*,#16501,.F.);
#22993=ORIENTED_EDGE('',*,*,#16500,.F.);
#22994=ORIENTED_EDGE('',*,*,#16502,.F.);
#22995=ORIENTED_EDGE('',*,*,#16501,.T.);
#22996=ORIENTED_EDGE('',*,*,#16503,.F.);
#22997=ORIENTED_EDGE('',*,*,#16504,.T.);
#22998=ORIENTED_EDGE('',*,*,#16502,.T.);
#22999=ORIENTED_EDGE('',*,*,#16504,.F.);
#23000=ORIENTED_EDGE('',*,*,#16503,.T.);
#23001=ORIENTED_EDGE('',*,*,#16499,.F.);
#26675=ADVANCED_FACE('',(#7851),#6692,.F.);
#26676=ADVANCED_FACE('',(#7852,#702),#1395,.T.);
#26677=ADVANCED_FACE('',(#7853),#6693,.T.);
#26678=ADVANCED_FACE('',(#7854,#703),#1396,.T.);
#27230=CLOSED_SHELL('',(#26675,#26676,#26677,#26678));
#29187=AXIS2_PLACEMENT_3D('',#45259,#35006,#35007);
#29188=AXIS2_PLACEMENT_3D('',#45260,#35008,#35009);
#29189=AXIS2_PLACEMENT_3D('',#45262,#35010,#35011);
#29190=AXIS2_PLACEMENT_3D('',#45265,#35013,#35014);
#29191=AXIS2_PLACEMENT_3D('',#45266,#35015,#35016);
#29192=AXIS2_PLACEMENT_3D('',#45268,#35017,#35018);
#29193=AXIS2_PLACEMENT_3D('',#45269,#35019,#35020);
#29194=AXIS2_PLACEMENT_3D('',#45271,#35021,#35022);
#29195=AXIS2_PLACEMENT_3D('',#45273,#35024,#35025);
#35006=DIRECTION('axis',(0.,0.,1.));
#35007=DIRECTION('refdir',(1.,0.,0.));
#35008=DIRECTION('center_axis',(1.,0.,0.));
#35009=DIRECTION('ref_axis',(0.,1.,0.));
#35010=DIRECTION('center_axis',(1.,0.,0.));
#35011=DIRECTION('ref_axis',(0.,0.,-1.));
#35012=DIRECTION('',(-1.,0.,0.));
#35013=DIRECTION('center_axis',(1.,0.,0.));
#35014=DIRECTION('ref_axis',(0.,0.,-1.));
#35015=DIRECTION('center_axis',(-1.,0.,0.));
#35016=DIRECTION('ref_axis',(0.,0.,1.));
#35017=DIRECTION('center_axis',(1.,0.,0.));
#35018=DIRECTION('ref_axis',(0.,0.,-1.));
#35019=DIRECTION('center_axis',(1.,0.,0.));
#35020=DIRECTION('ref_axis',(0.,1.,0.));
#35021=DIRECTION('center_axis',(1.,0.,0.));
#35022=DIRECTION('ref_axis',(0.,0.,-1.));
#35023=DIRECTION('',(-1.,0.,0.));
#35024=DIRECTION('center_axis',(1.,0.,0.));
#35025=DIRECTION('ref_axis',(0.,0.,-1.));
#45259=CARTESIAN_POINT('',(0.,0.,0.));
#45260=CARTESIAN_POINT('Origin',(0.25,0.,0.));
#45261=CARTESIAN_POINT('',(0.5,-12.55,-1.53693173292993E-15));
#45262=CARTESIAN_POINT('Origin',(0.5,0.,0.));
#45263=CARTESIAN_POINT('',(0.,-12.55,-1.53693173292993E-15));
#45264=CARTESIAN_POINT('',(0.25,-12.55,-1.53693173292993E-15));
#45265=CARTESIAN_POINT('Origin',(0.,0.,0.));
#45266=CARTESIAN_POINT('Origin',(0.,16.,0.));
#45267=CARTESIAN_POINT('',(0.,-16.,-1.95943487863577E-15));
#45268=CARTESIAN_POINT('Origin',(0.,0.,0.));
#45269=CARTESIAN_POINT('Origin',(0.25,0.,0.));
#45270=CARTESIAN_POINT('',(0.5,-16.,-1.95943487863577E-15));
#45271=CARTESIAN_POINT('Origin',(0.5,0.,0.));
#45272=CARTESIAN_POINT('',(0.25,-16.,-1.95943487863577E-15));
#45273=CARTESIAN_POINT('Origin',(0.5,12.55,0.));
#55704=UNCERTAINTY_MEASURE_WITH_UNIT(LENGTH_MEASURE(0.01),#55738,
'DISTANCE_ACCURACY_VALUE',
'Maximum model space distance between geometric entities at asserted c
onnectivities');
#55715=UNCERTAINTY_MEASURE_WITH_UNIT(LENGTH_MEASURE(0.01),#55738,
'DISTANCE_ACCURACY_VALUE',
'Maximum model space distance between geometric entities at asserted c
onnectivities');
#55726=(
GEOMETRIC_REPRESENTATION_CONTEXT(3)
GLOBAL_UNCERTAINTY_ASSIGNED_CONTEXT((#55704))
GLOBAL_UNIT_ASSIGNED_CONTEXT((#55738,#55740,#55741))
REPRESENTATION_CONTEXT('','3D')
);
#55737=(
GEOMETRIC_REPRESENTATION_CONTEXT(3)
GLOBAL_UNCERTAINTY_ASSIGNED_CONTEXT((#55715))
GLOBAL_UNIT_ASSIGNED_CONTEXT((#55738,#55740,#55741))
REPRESENTATION_CONTEXT('','3D')
);
#55738=(
LENGTH_UNIT()
NAMED_UNIT(*)
SI_UNIT(.MILLI.,.METRE.)
);
#55740=(
NAMED_UNIT(*)
PLANE_ANGLE_UNIT()
SI_UNIT($,.RADIAN.)
);
#55741=(
NAMED_UNIT(*)
SI_UNIT($,.STERADIAN.)
SOLID_ANGLE_UNIT()
);
#55752=SHAPE_DEFINITION_REPRESENTATION(#55773,#55830);
#55773=PRODUCT_DEFINITION_SHAPE('',$,#55852);
#55830=SHAPE_REPRESENTATION('',(#29187),#55726);
#55841=PRODUCT_DEFINITION_CONTEXT('part definition',#55906,'design');
#55852=PRODUCT_DEFINITION('2026-10-26-00-34-25-749',
'10_Axial_Preload_Shim_25x32x0.5',#55873,#55841);
#55873=PRODUCT_DEFINITION_FORMATION('',$,#55918);
#55906=APPLICATION_CONTEXT(
'Core Data for Automotive Mechanical Design Process');
#55907=PRODUCT_CONTEXT('part definition',#55906,'mechanical');
#55918=PRODUCT('2026-10-26-00-34-25-749',
'10_Axial_Preload_Shim_25x32x0.5',$,(#55907));
#55999=COLOUR_RGB('Off White',0.89,0.88,0.83);
#56000=FILL_AREA_STYLE_COLOUR('',#55999);
#56001=FILL_AREA_STYLE('',(#56000));
#56002=SURFACE_STYLE_FILL_AREA(#56001);
#56003=SURFACE_SIDE_STYLE('',(#56002));
#56004=SURFACE_STYLE_USAGE(.BOTH.,#56003);
#56005=PRESENTATION_STYLE_ASSIGNMENT((#56004));
ENDSEC;
END-ISO-10303-21;
